ISO-10303-21;
HEADER;
/* Generated by software containing ST-Developer
 * from STEP Tools, Inc. (www.steptools.com) 
 */

FILE_DESCRIPTION(
/* description */ ('Cylinder foot and clevis mount kit'),
/* implementation_level */ '2;1');

FILE_NAME(
/* name */ 'Socket Set Screw - M4x6.step',
/* time_stamp */ '2026-10-27T20:10:43-07:00',
/* author */ (''),
/* organization */ (''),
/* preprocessor_version */ 'ST-DEVELOPER v20.2',
/* originating_system */ 'Autodesk Translation Framework v15.17.0.0',
/* authorisation */ '');

FILE_SCHEMA (('AUTOMOTIVE_DESIGN { 1 0 10303 214 3 1 1 }'));
ENDSEC;

DATA;
#10=MECHANICAL_DESIGN_GEOMETRIC_PRESENTATION_REPRESENTATION('',(#362),#9102);
#278=CONICAL_SURFACE('',#5836,0.185,0.785398163397449);
#279=CONICAL_SURFACE('',#5840,0.1625,0.785398163397449);
#306=SHAPE_REPRESENTATION_RELATIONSHIP('SRR','None',#9255,#334);
#334=ADVANCED_BREP_SHAPE_REPRESENTATION('',(#388),#9098);
#362=STYLED_ITEM('',(#9467),#388);
#388=MANIFOLD_SOLID_BREP('Body1',#4950);
#489=FACE_BOUND('',#1383,.T.);
#678=PLANE('',#5827);
#679=PLANE('',#5828);
#680=PLANE('',#5829);
#681=PLANE('',#5830);
#682=PLANE('',#5831);
#683=PLANE('',#5832);
#684=PLANE('',#5833);
#685=PLANE('',#5834);
#686=PLANE('',#5842);
#972=FACE_OUTER_BOUND('',#1375,.T.);
#973=FACE_OUTER_BOUND('',#1376,.T.);
#974=FACE_OUTER_BOUND('',#1377,.T.);
#975=FACE_OUTER_BOUND('',#1378,.T.);
#976=FACE_OUTER_BOUND('',#1379,.T.);
#977=FACE_OUTER_BOUND('',#1380,.T.);
#978=FACE_OUTER_BOUND('',#1381,.T.);
#979=FACE_OUTER_BOUND('',#1382,.T.);
#980=FACE_OUTER_BOUND('',#1384,.T.);
#981=FACE_OUTER_BOUND('',#1385,.T.);
#982=FACE_OUTER_BOUND('',#1386,.T.);
#983=FACE_OUTER_BOUND('',#1387,.T.);
#1375=EDGE_LOOP('',(#4403,#4404,#4405,#4406));
#1376=EDGE_LOOP('',(#4407,#4408,#4409,#4410));
#1377=EDGE_LOOP('',(#4411,#4412,#4413,#4414));
#1378=EDGE_LOOP('',(#4415,#4416,#4417,#4418));
#1379=EDGE_LOOP('',(#4419,#4420,#4421,#4422));
#1380=EDGE_LOOP('',(#4423,#4424,#4425,#4426));
#1381=EDGE_LOOP('',(#4427,#4428,#4429,#4430,#4431,#4432));
#1382=EDGE_LOOP('',(#4433));
#1383=EDGE_LOOP('',(#4434,#4435,#4436,#4437,#4438,#4439));
#1384=EDGE_LOOP('',(#4440,#4441,#4442,#4443));
#1385=EDGE_LOOP('',(#4444,#4445,#4446,#4447));
#1386=EDGE_LOOP('',(#4448,#4449,#4450,#4451));
#1387=EDGE_LOOP('',(#4452));
#1725=LINE('',#8780,#2074);
#1726=LINE('',#8782,#2075);
#1727=LINE('',#8784,#2076);
#1728=LINE('',#8785,#2077);
#1729=LINE('',#8788,#2078);
#1730=LINE('',#8790,#2079);
#1731=LINE('',#8791,#2080);
#1732=LINE('',#8794,#2081);
#1733=LINE('',#8796,#2082);
#1734=LINE('',#8797,#2083);
#1735=LINE('',#8800,#2084);
#1736=LINE('',#8802,#2085);
#1737=LINE('',#8803,#2086);
#1738=LINE('',#8806,#2087);
#1739=LINE('',#8808,#2088);
#1740=LINE('',#8809,#2089);
#1741=LINE('',#8811,#2090);
#1742=LINE('',#8812,#2091);
#1743=LINE('',#8820,#2092);
#1744=LINE('',#8824,#2093);
#1745=LINE('',#8828,#2094);
#2074=VECTOR('',#7336,1.);
#2075=VECTOR('',#7337,1.);
#2076=VECTOR('',#7338,1.);
#2077=VECTOR('',#7339,1.);
#2078=VECTOR('',#7342,1.);
#2079=VECTOR('',#7343,1.);
#2080=VECTOR('',#7344,1.);
#2081=VECTOR('',#7347,1.);
#2082=VECTOR('',#7348,1.);
#2083=VECTOR('',#7349,1.);
#2084=VECTOR('',#7352,1.);
#2085=VECTOR('',#7353,1.);
#2086=VECTOR('',#7354,1.);
#2087=VECTOR('',#7357,1.);
#2088=VECTOR('',#7358,1.);
#2089=VECTOR('',#7359,1.);
#2090=VECTOR('',#7362,1.);
#2091=VECTOR('',#7363,1.);
#2092=VECTOR('',#7374,0.185);
#2093=VECTOR('',#7379,0.2);
#2094=VECTOR('',#7384,0.1625);
#2309=CIRCLE('',#5835,0.17);
#2310=CIRCLE('',#5837,0.1954);
#2311=CIRCLE('',#5839,0.1954);
#2312=CIRCLE('',#5841,0.125);
#2674=VERTEX_POINT('',#8778);
#2675=VERTEX_POINT('',#8779);
#2676=VERTEX_POINT('',#8781);
#2677=VERTEX_POINT('',#8783);
#2678=VERTEX_POINT('',#8787);
#2679=VERTEX_POINT('',#8789);
#2680=VERTEX_POINT('',#8793);
#2681=VERTEX_POINT('',#8795);
#2682=VERTEX_POINT('',#8799);
#2683=VERTEX_POINT('',#8801);
#2684=VERTEX_POINT('',#8805);
#2685=VERTEX_POINT('',#8807);
#2686=VERTEX_POINT('',#8815);
#2687=VERTEX_POINT('',#8818);
#2688=VERTEX_POINT('',#8822);
#2689=VERTEX_POINT('',#8826);
#3256=EDGE_CURVE('',#2674,#2675,#1725,.T.);
#3257=EDGE_CURVE('',#2674,#2676,#1726,.T.);
#3258=EDGE_CURVE('',#2676,#2677,#1727,.T.);
#3259=EDGE_CURVE('',#2675,#2677,#1728,.T.);
#3260=EDGE_CURVE('',#2678,#2674,#1729,.T.);
#3261=EDGE_CURVE('',#2678,#2679,#1730,.T.);
#3262=EDGE_CURVE('',#2679,#2676,#1731,.T.);
#3263=EDGE_CURVE('',#2680,#2678,#1732,.T.);
#3264=EDGE_CURVE('',#2680,#2681,#1733,.T.);
#3265=EDGE_CURVE('',#2681,#2679,#1734,.T.);
#3266=EDGE_CURVE('',#2682,#2680,#1735,.T.);
#3267=EDGE_CURVE('',#2682,#2683,#1736,.T.);
#3268=EDGE_CURVE('',#2683,#2681,#1737,.T.);
#3269=EDGE_CURVE('',#2684,#2682,#1738,.T.);
#3270=EDGE_CURVE('',#2684,#2685,#1739,.T.);
#3271=EDGE_CURVE('',#2685,#2683,#1740,.T.);
#3272=EDGE_CURVE('',#2675,#2684,#1741,.T.);
#3273=EDGE_CURVE('',#2677,#2685,#1742,.T.);
#3274=EDGE_CURVE('',#2686,#2686,#2309,.T.);
#3275=EDGE_CURVE('',#2687,#2687,#2310,.T.);
#3276=EDGE_CURVE('',#2687,#2686,#1743,.T.);
#3277=EDGE_CURVE('',#2688,#2688,#2311,.F.);
#3278=EDGE_CURVE('',#2688,#2687,#1744,.T.);
#3279=EDGE_CURVE('',#2689,#2689,#2312,.T.);
#3280=EDGE_CURVE('',#2689,#2688,#1745,.T.);
#4403=ORIENTED_EDGE('',*,*,#3256,.F.);
#4404=ORIENTED_EDGE('',*,*,#3257,.T.);
#4405=ORIENTED_EDGE('',*,*,#3258,.T.);
#4406=ORIENTED_EDGE('',*,*,#3259,.F.);
#4407=ORIENTED_EDGE('',*,*,#3260,.F.);
#4408=ORIENTED_EDGE('',*,*,#3261,.T.);
#4409=ORIENTED_EDGE('',*,*,#3262,.T.);
#4410=ORIENTED_EDGE('',*,*,#3257,.F.);
#4411=ORIENTED_EDGE('',*,*,#3263,.F.);
#4412=ORIENTED_EDGE('',*,*,#3264,.T.);
#4413=ORIENTED_EDGE('',*,*,#3265,.T.);
#4414=ORIENTED_EDGE('',*,*,#3261,.F.);
#4415=ORIENTED_EDGE('',*,*,#3266,.F.);
#4416=ORIENTED_EDGE('',*,*,#3267,.T.);
#4417=ORIENTED_EDGE('',*,*,#3268,.T.);
#4418=ORIENTED_EDGE('',*,*,#3264,.F.);
#4419=ORIENTED_EDGE('',*,*,#3269,.F.);
#4420=ORIENTED_EDGE('',*,*,#3270,.T.);
#4421=ORIENTED_EDGE('',*,*,#3271,.T.);
#4422=ORIENTED_EDGE('',*,*,#3267,.F.);
#4423=ORIENTED_EDGE('',*,*,#3272,.F.);
#4424=ORIENTED_EDGE('',*,*,#3259,.T.);
#4425=ORIENTED_EDGE('',*,*,#3273,.T.);
#4426=ORIENTED_EDGE('',*,*,#3270,.F.);
#4427=ORIENTED_EDGE('',*,*,#3273,.F.);
#4428=ORIENTED_EDGE('',*,*,#3258,.F.);
#4429=ORIENTED_EDGE('',*,*,#3262,.F.);
#4430=ORIENTED_EDGE('',*,*,#3265,.F.);
#4431=ORIENTED_EDGE('',*,*,#3268,.F.);
#4432=ORIENTED_EDGE('',*,*,#3271,.F.);
#4433=ORIENTED_EDGE('',*,*,#3274,.F.);
#4434=ORIENTED_EDGE('',*,*,#3256,.T.);
#4435=ORIENTED_EDGE('',*,*,#3272,.T.);
#4436=ORIENTED_EDGE('',*,*,#3269,.T.);
#4437=ORIENTED_EDGE('',*,*,#3266,.T.);
#4438=ORIENTED_EDGE('',*,*,#3263,.T.);
#4439=ORIENTED_EDGE('',*,*,#3260,.T.);
#4440=ORIENTED_EDGE('',*,*,#3275,.F.);
#4441=ORIENTED_EDGE('',*,*,#3276,.T.);
#4442=ORIENTED_EDGE('',*,*,#3274,.T.);
#4443=ORIENTED_EDGE('',*,*,#3276,.F.);
#4444=ORIENTED_EDGE('',*,*,#3277,.F.);
#4445=ORIENTED_EDGE('',*,*,#3278,.T.);
#4446=ORIENTED_EDGE('',*,*,#3275,.T.);
#4447=ORIENTED_EDGE('',*,*,#3278,.F.);
#4448=ORIENTED_EDGE('',*,*,#3279,.F.);
#4449=ORIENTED_EDGE('',*,*,#3280,.T.);
#4450=ORIENTED_EDGE('',*,*,#3277,.T.);
#4451=ORIENTED_EDGE('',*,*,#3280,.F.);
#4452=ORIENTED_EDGE('',*,*,#3279,.T.);
#4611=CYLINDRICAL_SURFACE('',#5838,0.1954);
#4895=ADVANCED_FACE('',(#972),#678,.F.);
#4896=ADVANCED_FACE('',(#973),#679,.F.);
#4897=ADVANCED_FACE('',(#974),#680,.F.);
#4898=ADVANCED_FACE('',(#975),#681,.F.);
#4899=ADVANCED_FACE('',(#976),#682,.F.);
#4900=ADVANCED_FACE('',(#977),#683,.F.);
#4901=ADVANCED_FACE('',(#978),#684,.F.);
#4902=ADVANCED_FACE('',(#979,#489),#685,.T.);
#4903=ADVANCED_FACE('',(#980),#278,.T.);
#4904=ADVANCED_FACE('',(#981),#4611,.T.);
#4905=ADVANCED_FACE('',(#982),#279,.T.);
#4906=ADVANCED_FACE('',(#983),#686,.T.);
#4950=CLOSED_SHELL('',(#4895,#4896,#4897,#4898,#4899,#4900,#4901,#4902,
#4903,#4904,#4905,#4906));
#5826=AXIS2_PLACEMENT_3D('',#8776,#7332,#7333);
#5827=AXIS2_PLACEMENT_3D('',#8777,#7334,#7335);
#5828=AXIS2_PLACEMENT_3D('',#8786,#7340,#7341);
#5829=AXIS2_PLACEMENT_3D('',#8792,#7345,#7346);
#5830=AXIS2_PLACEMENT_3D('',#8798,#7350,#7351);
#5831=AXIS2_PLACEMENT_3D('',#8804,#7355,#7356);
#5832=AXIS2_PLACEMENT_3D('',#8810,#7360,#7361);
#5833=AXIS2_PLACEMENT_3D('',#8813,#7364,#7365);
#5834=AXIS2_PLACEMENT_3D('',#8814,#7366,#7367);
#5835=AXIS2_PLACEMENT_3D('',#8816,#7368,#7369);
#5836=AXIS2_PLACEMENT_3D('',#8817,#7370,#7371);
#5837=AXIS2_PLACEMENT_3D('',#8819,#7372,#7373);
#5838=AXIS2_PLACEMENT_3D('',#8821,#7375,#7376);
#5839=AXIS2_PLACEMENT_3D('',#8823,#7377,#7378);
#5840=AXIS2_PLACEMENT_3D('',#8825,#7380,#7381);
#5841=AXIS2_PLACEMENT_3D('',#8827,#7382,#7383);
#5842=AXIS2_PLACEMENT_3D('',#8829,#7385,#7386);
#7332=DIRECTION('axis',(0.,0.,1.));
#7333=DIRECTION('refdir',(1.,0.,0.));
#7334=DIRECTION('center_axis',(0.866025403784439,0.,-0.5));
#7335=DIRECTION('ref_axis',(0.5,0.,0.866025403784439));
#7336=DIRECTION('',(0.5,0.,0.866025403784439));
#7337=DIRECTION('',(0.,-1.,0.));
#7338=DIRECTION('',(0.5,0.,0.866025403784439));
#7339=DIRECTION('',(0.,-1.,0.));
#7340=DIRECTION('center_axis',(1.20185167898973E-16,0.,-1.));
#7341=DIRECTION('ref_axis',(1.,0.,1.20185167898973E-16));
#7342=DIRECTION('',(1.,0.,1.20185167898973E-16));
#7343=DIRECTION('',(0.,-1.,0.));
#7344=DIRECTION('',(1.,0.,1.20185167898973E-16));
#7345=DIRECTION('center_axis',(-0.866025403784439,0.,-0.5));
#7346=DIRECTION('ref_axis',(0.5,0.,-0.866025403784439));
#7347=DIRECTION('',(0.5,0.,-0.866025403784439));
#7348=DIRECTION('',(0.,-1.,0.));
#7349=DIRECTION('',(0.5,0.,-0.866025403784439));
#7350=DIRECTION('center_axis',(-0.866025403784439,0.,0.5));
#7351=DIRECTION('ref_axis',(-0.5,0.,-0.866025403784439));
#7352=DIRECTION('',(-0.5,0.,-0.866025403784439));
#7353=DIRECTION('',(0.,-1.,0.));
#7354=DIRECTION('',(-0.5,0.,-0.866025403784439));
#7355=DIRECTION('center_axis',(-2.40370335797945E-16,0.,1.));
#7356=DIRECTION('ref_axis',(-1.,0.,-2.40370335797945E-16));
#7357=DIRECTION('',(-1.,0.,-2.40370335797945E-16));
#7358=DIRECTION('',(0.,-1.,0.));
#7359=DIRECTION('',(-1.,0.,-2.40370335797945E-16));
#7360=DIRECTION('center_axis',(0.866025403784439,0.,0.5));
#7361=DIRECTION('ref_axis',(-0.5,0.,0.866025403784439));
#7362=DIRECTION('',(-0.5,0.,0.866025403784439));
#7363=DIRECTION('',(-0.5,0.,0.866025403784439));
#7364=DIRECTION('center_axis',(0.,-1.,0.));
#7365=DIRECTION('ref_axis',(0.,0.,-1.));
#7366=DIRECTION('center_axis',(0.,1.,0.));
#7367=DIRECTION('ref_axis',(0.,0.,1.));
#7368=DIRECTION('center_axis',(0.,-1.,0.));
#7369=DIRECTION('ref_axis',(1.,0.,0.));
#7370=DIRECTION('center_axis',(0.,-1.,0.));
#7371=DIRECTION('ref_axis',(1.,0.,0.));
#7372=DIRECTION('center_axis',(0.,-1.,0.));
#7373=DIRECTION('ref_axis',(1.,0.,0.));
#7374=DIRECTION('',(0.707106781186548,0.707106781186547,8.65956056235494E-17));
#7375=DIRECTION('center_axis',(0.,-1.,0.));
#7376=DIRECTION('ref_axis',(1.,0.,0.));
#7377=DIRECTION('center_axis',(0.,1.,0.));
#7378=DIRECTION('ref_axis',(1.,0.,0.));
#7379=DIRECTION('',(0.,1.,0.));
#7380=DIRECTION('center_axis',(0.,1.,0.));
#7381=DIRECTION('ref_axis',(1.,0.,0.));
#7382=DIRECTION('center_axis',(0.,-1.,0.));
#7383=DIRECTION('ref_axis',(1.,0.,0.));
#7384=DIRECTION('',(-0.707106781186548,0.707106781186547,-8.65956056235494E-17));
#7385=DIRECTION('center_axis',(0.,-1.,0.));
#7386=DIRECTION('ref_axis',(0.,0.,-1.));
#8776=CARTESIAN_POINT('',(0.,0.,0.));
#8777=CARTESIAN_POINT('Origin',(0.0577350269189626,0.,-0.1));
#8778=CARTESIAN_POINT('',(0.0577350269189626,0.,-0.1));
#8779=CARTESIAN_POINT('',(0.115470053837925,0.,0.));
#8780=CARTESIAN_POINT('',(0.0934187836487032,0.,-0.0381939203391614));
#8781=CARTESIAN_POINT('',(0.0577350269189626,-0.2,-0.1));
#8782=CARTESIAN_POINT('',(0.0577350269189626,0.,-0.1));
#8783=CARTESIAN_POINT('',(0.115470053837925,-0.2,0.));
#8784=CARTESIAN_POINT('',(0.115470053837925,-0.2,0.));
#8785=CARTESIAN_POINT('',(0.115470053837925,0.,0.));
#8786=CARTESIAN_POINT('Origin',(-0.0577350269189626,0.,-0.1));
#8787=CARTESIAN_POINT('',(-0.0577350269189626,0.,-0.1));
#8788=CARTESIAN_POINT('',(0.0561324865405187,0.,-0.1));
#8789=CARTESIAN_POINT('',(-0.0577350269189626,-0.2,-0.1));
#8790=CARTESIAN_POINT('',(-0.0577350269189626,0.,-0.1));
#8791=CARTESIAN_POINT('',(0.0577350269189626,-0.2,-0.1));
#8792=CARTESIAN_POINT('Origin',(-0.115470053837925,0.,-1.38777878078145E-17));
#8793=CARTESIAN_POINT('',(-0.115470053837925,0.,-1.41410031829988E-17));
#8794=CARTESIAN_POINT('',(-0.0797862971081845,0.,-0.0618060796608387));
#8795=CARTESIAN_POINT('',(-0.115470053837925,-0.2,-1.38777878078145E-17));
#8796=CARTESIAN_POINT('',(-0.115470053837925,0.,-1.41410031829988E-17));
#8797=CARTESIAN_POINT('',(-0.0577350269189626,-0.2,-0.1));
#8798=CARTESIAN_POINT('Origin',(-0.0577350269189626,0.,0.1));
#8799=CARTESIAN_POINT('',(-0.0577350269189626,0.,0.1));
#8800=CARTESIAN_POINT('',(-0.0509187836487033,0.,0.111806079660839));
#8801=CARTESIAN_POINT('',(-0.0577350269189626,-0.2,0.1));
#8802=CARTESIAN_POINT('',(-0.0577350269189626,0.,0.1));
#8803=CARTESIAN_POINT('',(-0.115470053837925,-0.2,-1.41410031829988E-17));
#8804=CARTESIAN_POINT('Origin',(0.0577350269189626,0.,0.1));
#8805=CARTESIAN_POINT('',(0.0577350269189626,0.,0.1));
#8806=CARTESIAN_POINT('',(0.113867513459481,0.,0.1));
#8807=CARTESIAN_POINT('',(0.0577350269189626,-0.2,0.1));
#8808=CARTESIAN_POINT('',(0.0577350269189626,0.,0.1));
#8809=CARTESIAN_POINT('',(-0.0577350269189626,-0.2,0.1));
#8810=CARTESIAN_POINT('Origin',(0.115470053837925,0.,0.));
#8811=CARTESIAN_POINT('',(0.122286297108185,0.,-0.0118060796608386));
#8812=CARTESIAN_POINT('',(0.0577350269189626,-0.2,0.1));
#8813=CARTESIAN_POINT('Origin',(0.,-0.2,0.));
#8814=CARTESIAN_POINT('Origin',(0.17,0.,0.));
#8815=CARTESIAN_POINT('',(-0.17,-8.67361737988404E-18,-2.0818995585505E-17));
#8816=CARTESIAN_POINT('Origin',(0.,0.,0.));
#8817=CARTESIAN_POINT('Origin',(0.,-0.015,0.));
#8818=CARTESIAN_POINT('',(-0.1954,-0.0254,-2.39295984553393E-17));
#8819=CARTESIAN_POINT('Origin',(0.,-0.0254,0.));
#8820=CARTESIAN_POINT('',(-0.185,-0.015,-2.2655965784226E-17));
#8821=CARTESIAN_POINT('Origin',(0.,-0.2775,0.));
#8822=CARTESIAN_POINT('',(-0.1954,-0.5296,2.39295984553393E-17));
#8823=CARTESIAN_POINT('Origin',(0.,-0.5296,0.));
#8824=CARTESIAN_POINT('',(-0.1954,-0.2775,-2.39295984553393E-17));
#8825=CARTESIAN_POINT('Origin',(0.,-0.5625,0.));
#8826=CARTESIAN_POINT('',(-0.125,-0.6,-1.53080849893419E-17));
#8827=CARTESIAN_POINT('Origin',(0.,-0.6,0.));
#8828=CARTESIAN_POINT('',(-0.1625,-0.5625,-1.99005104861445E-17));
#8829=CARTESIAN_POINT('Origin',(0.,-0.6,0.));
#9065=UNCERTAINTY_MEASURE_WITH_UNIT(LENGTH_MEASURE(0.001),#9103,
'DISTANCE_ACCURACY_VALUE',
'Maximum model space distance between geometric entities at asserted c
onnectivities');
#9069=UNCERTAINTY_MEASURE_WITH_UNIT(LENGTH_MEASURE(0.001),#9103,
'DISTANCE_ACCURACY_VALUE',
'Maximum model space distance between geometric entities at asserted c
onnectivities');
#9098=(
GEOMETRIC_REPRESENTATION_CONTEXT(3)
GLOBAL_UNCERTAINTY_ASSIGNED_CONTEXT((#9065))
GLOBAL_UNIT_ASSIGNED_CONTEXT((#9103,#9105,#9106))
REPRESENTATION_CONTEXT('','3D')
);
#9102=(
GEOMETRIC_REPRESENTATION_CONTEXT(3)
GLOBAL_UNCERTAINTY_ASSIGNED_CONTEXT((#9069))
GLOBAL_UNIT_ASSIGNED_CONTEXT((#9103,#9105,#9106))
REPRESENTATION_CONTEXT('','3D')
);
#9103=(
LENGTH_UNIT()
NAMED_UNIT(*)
SI_UNIT(.CENTI.,.METRE.)
);
#9105=(
NAMED_UNIT(*)
PLANE_ANGLE_UNIT()
SI_UNIT($,.RADIAN.)
);
#9106=(
NAMED_UNIT(*)
SI_UNIT($,.STERADIAN.)
SOLID_ANGLE_UNIT()
);
#9135=SHAPE_DEFINITION_REPRESENTATION(#9210,#9255);
#9210=PRODUCT_DEFINITION_SHAPE('',$,#9288);
#9255=SHAPE_REPRESENTATION('',(#5826),#9098);
#9259=PRODUCT_DEFINITION_CONTEXT('part definition',#9357,'design');
#9288=PRODUCT_DEFINITION('Socket Set Screw - M4x6',
'Socket Set Screw - M4x6',#9320,#9259);
#9320=PRODUCT_DEFINITION_FORMATION('',$,#9387);
#9357=APPLICATION_CONTEXT(
'Core Data for Automotive Mechanical Design Process');
#9358=PRODUCT_CONTEXT('part definition',#9357,'mechanical');
#9387=PRODUCT('Socket Set Screw - M4x6','Socket Set Screw - M4x6',
'Socket Set Screw - M4x6',(#9358));
#9461=COLOUR_RGB('Black',0.12,0.14,0.17);
#9462=FILL_AREA_STYLE_COLOUR('',#9461);
#9463=FILL_AREA_STYLE('',(#9462));
#9464=SURFACE_STYLE_FILL_AREA(#9463);
#9465=SURFACE_SIDE_STYLE('',(#9464));
#9466=SURFACE_STYLE_USAGE(.BOTH.,#9465);
#9467=PRESENTATION_STYLE_ASSIGNMENT((#9466));
ENDSEC;
END-ISO-10303-21;
